ISO-10303-21;
HEADER;
/* Generated by software containing ST-Developer
 * from STEP Tools, Inc. (www.steptools.com) 
 */

FILE_DESCRIPTION(
/* description */ ('Wall-mounted air drop station'),
/* implementation_level */ '2;1');

FILE_NAME(
/* name */ 'Flat Washer - M5.step',
/* time_stamp */ '2026-10-28T22:16:19-07:00',
/* author */ (''),
/* organization */ (''),
/* preprocessor_version */ 'ST-DEVELOPER v20.2',
/* originating_system */ 'Autodesk Translation Framework v15.17.0.0',
/* authorisation */ '');

FILE_SCHEMA (('AUTOMOTIVE_DESIGN { 1 0 10303 214 3 1 1 }'));
ENDSEC;

DATA;
#10=MECHANICAL_DESIGN_GEOMETRIC_PRESENTATION_REPRESENTATION('',(#358),#10517);
#270=CONICAL_SURFACE('',#6594,0.275,0.785398163397449);
#300=SHAPE_REPRESENTATION_RELATIONSHIP('SRR','None',#10657,#329);
#329=ADVANCED_BREP_SHAPE_REPRESENTATION('',(#386),#10501);
#358=STYLED_ITEM('',(#10881),#386);
#386=MANIFOLD_SOLID_BREP('Body1',#5898);
#494=FACE_BOUND('',#1400,.T.);
#495=FACE_BOUND('',#1403,.T.);
#641=PLANE('',#6599);
#642=PLANE('',#6603);
#947=FACE_OUTER_BOUND('',#1397,.T.);
#948=FACE_OUTER_BOUND('',#1398,.T.);
#949=FACE_OUTER_BOUND('',#1399,.T.);
#950=FACE_OUTER_BOUND('',#1401,.T.);
#951=FACE_OUTER_BOUND('',#1402,.T.);
#1397=EDGE_LOOP('',(#4777,#4778,#4779,#4780));
#1398=EDGE_LOOP('',(#4781,#4782,#4783,#4784));
#1399=EDGE_LOOP('',(#4785));
#1400=EDGE_LOOP('',(#4786));
#1401=EDGE_LOOP('',(#4787,#4788,#4789,#4790));
#1402=EDGE_LOOP('',(#4791));
#1403=EDGE_LOOP('',(#4792));
#1844=LINE('',#9648,#2308);
#1845=LINE('',#9652,#2309);
#1846=LINE('',#9659,#2310);
#2308=VECTOR('',#7898,0.275);
#2309=VECTOR('',#7903,0.265);
#2310=VECTOR('',#7912,0.5);
#2670=CIRCLE('',#6595,0.285);
#2671=CIRCLE('',#6596,0.265);
#2672=CIRCLE('',#6598,0.265);
#2673=CIRCLE('',#6600,0.5);
#2674=CIRCLE('',#6602,0.5);
#3032=VERTEX_POINT('',#9645);
#3033=VERTEX_POINT('',#9647);
#3034=VERTEX_POINT('',#9651);
#3035=VERTEX_POINT('',#9655);
#3036=VERTEX_POINT('',#9658);
#3646=EDGE_CURVE('',#3032,#3032,#2670,.T.);
#3647=EDGE_CURVE('',#3032,#3033,#1844,.T.);
#3648=EDGE_CURVE('',#3033,#3033,#2671,.T.);
#3649=EDGE_CURVE('',#3033,#3034,#1845,.T.);
#3650=EDGE_CURVE('',#3034,#3034,#2672,.T.);
#3651=EDGE_CURVE('',#3035,#3035,#2673,.T.);
#3652=EDGE_CURVE('',#3035,#3036,#1846,.T.);
#3653=EDGE_CURVE('',#3036,#3036,#2674,.T.);
#4777=ORIENTED_EDGE('',*,*,#3646,.T.);
#4778=ORIENTED_EDGE('',*,*,#3647,.T.);
#4779=ORIENTED_EDGE('',*,*,#3648,.T.);
#4780=ORIENTED_EDGE('',*,*,#3647,.F.);
#4781=ORIENTED_EDGE('',*,*,#3648,.F.);
#4782=ORIENTED_EDGE('',*,*,#3649,.T.);
#4783=ORIENTED_EDGE('',*,*,#3650,.T.);
#4784=ORIENTED_EDGE('',*,*,#3649,.F.);
#4785=ORIENTED_EDGE('',*,*,#3651,.T.);
#4786=ORIENTED_EDGE('',*,*,#3646,.F.);
#4787=ORIENTED_EDGE('',*,*,#3651,.F.);
#4788=ORIENTED_EDGE('',*,*,#3652,.T.);
#4789=ORIENTED_EDGE('',*,*,#3653,.T.);
#4790=ORIENTED_EDGE('',*,*,#3652,.F.);
#4791=ORIENTED_EDGE('',*,*,#3653,.F.);
#4792=ORIENTED_EDGE('',*,*,#3650,.F.);
#5498=CYLINDRICAL_SURFACE('',#6597,0.265);
#5499=CYLINDRICAL_SURFACE('',#6601,0.5);
#5720=ADVANCED_FACE('',(#947),#270,.F.);
#5721=ADVANCED_FACE('',(#948),#5498,.F.);
#5722=ADVANCED_FACE('',(#949,#494),#641,.T.);
#5723=ADVANCED_FACE('',(#950),#5499,.T.);
#5724=ADVANCED_FACE('',(#951,#495),#642,.F.);
#5898=CLOSED_SHELL('',(#5720,#5721,#5722,#5723,#5724));
#6593=AXIS2_PLACEMENT_3D('',#9643,#7892,#7893);
#6594=AXIS2_PLACEMENT_3D('',#9644,#7894,#7895);
#6595=AXIS2_PLACEMENT_3D('',#9646,#7896,#7897);
#6596=AXIS2_PLACEMENT_3D('',#9649,#7899,#7900);
#6597=AXIS2_PLACEMENT_3D('',#9650,#7901,#7902);
#6598=AXIS2_PLACEMENT_3D('',#9653,#7904,#7905);
#6599=AXIS2_PLACEMENT_3D('',#9654,#7906,#7907);
#6600=AXIS2_PLACEMENT_3D('',#9656,#7908,#7909);
#6601=AXIS2_PLACEMENT_3D('',#9657,#7910,#7911);
#6602=AXIS2_PLACEMENT_3D('',#9660,#7913,#7914);
#6603=AXIS2_PLACEMENT_3D('',#9661,#7915,#7916);
#7892=DIRECTION('axis',(0.,0.,1.));
#7893=DIRECTION('refdir',(1.,0.,0.));
#7894=DIRECTION('center_axis',(0.,1.,0.));
#7895=DIRECTION('ref_axis',(1.,0.,0.));
#7896=DIRECTION('center_axis',(0.,1.,0.));
#7897=DIRECTION('ref_axis',(1.,0.,0.));
#7898=DIRECTION('',(0.707106781186548,-0.707106781186547,-8.65956056235494E-17));
#7899=DIRECTION('center_axis',(0.,-1.,0.));
#7900=DIRECTION('ref_axis',(1.,0.,0.));
#7901=DIRECTION('center_axis',(0.,1.,0.));
#7902=DIRECTION('ref_axis',(1.,0.,0.));
#7903=DIRECTION('',(0.,-1.,0.));
#7904=DIRECTION('center_axis',(0.,-1.,0.));
#7905=DIRECTION('ref_axis',(1.,0.,0.));
#7906=DIRECTION('center_axis',(0.,1.,0.));
#7907=DIRECTION('ref_axis',(1.,0.,0.));
#7908=DIRECTION('center_axis',(0.,1.,0.));
#7909=DIRECTION('ref_axis',(1.,0.,0.));
#7910=DIRECTION('center_axis',(0.,1.,0.));
#7911=DIRECTION('ref_axis',(1.,0.,0.));
#7912=DIRECTION('',(0.,-1.,0.));
#7913=DIRECTION('center_axis',(0.,1.,0.));
#7914=DIRECTION('ref_axis',(1.,0.,0.));
#7915=DIRECTION('center_axis',(0.,1.,0.));
#7916=DIRECTION('ref_axis',(1.,0.,0.));
#9643=CARTESIAN_POINT('',(0.,0.,0.));
#9644=CARTESIAN_POINT('Origin',(0.,0.09,0.));
#9645=CARTESIAN_POINT('',(-0.285,0.1,3.49024337756996E-17));
#9646=CARTESIAN_POINT('Origin',(0.,0.1,0.));
#9647=CARTESIAN_POINT('',(-0.265,0.08,-3.24531401774049E-17));
#9648=CARTESIAN_POINT('',(-0.275,0.09,3.36777869765522E-17));
#9649=CARTESIAN_POINT('Origin',(0.,0.08,0.));
#9650=CARTESIAN_POINT('Origin',(0.,0.,0.));
#9651=CARTESIAN_POINT('',(-0.265,0.,3.24531401774049E-17));
#9652=CARTESIAN_POINT('',(-0.265,0.,3.24531401774049E-17));
#9653=CARTESIAN_POINT('Origin',(0.,0.,0.));
#9654=CARTESIAN_POINT('Origin',(0.,0.1,0.));
#9655=CARTESIAN_POINT('',(-0.5,0.1,6.12323399573677E-17));
#9656=CARTESIAN_POINT('Origin',(0.,0.1,0.));
#9657=CARTESIAN_POINT('Origin',(0.,0.,0.));
#9658=CARTESIAN_POINT('',(-0.5,0.,6.12323399573677E-17));
#9659=CARTESIAN_POINT('',(-0.5,0.,6.12323399573677E-17));
#9660=CARTESIAN_POINT('Origin',(0.,0.,0.));
#9661=CARTESIAN_POINT('Origin',(0.,0.,0.));
#10468=UNCERTAINTY_MEASURE_WITH_UNIT(LENGTH_MEASURE(0.001),#10518,
'DISTANCE_ACCURACY_VALUE',
'Maximum model space distance between geometric entities at asserted c
onnectivities');
#10484=UNCERTAINTY_MEASURE_WITH_UNIT(LENGTH_MEASURE(0.001),#10518,
'DISTANCE_ACCURACY_VALUE',
'Maximum model space distance between geometric entities at asserted c
onnectivities');
#10501=(
GEOMETRIC_REPRESENTATION_CONTEXT(3)
GLOBAL_UNCERTAINTY_ASSIGNED_CONTEXT((#10468))
GLOBAL_UNIT_ASSIGNED_CONTEXT((#10518,#10520,#10521))
REPRESENTATION_CONTEXT('','3D')
);
#10517=(
GEOMETRIC_REPRESENTATION_CONTEXT(3)
GLOBAL_UNCERTAINTY_ASSIGNED_CONTEXT((#10484))
GLOBAL_UNIT_ASSIGNED_CONTEXT((#10518,#10520,#10521))
REPRESENTATION_CONTEXT('','3D')
);
#10518=(
LENGTH_UNIT()
NAMED_UNIT(*)
SI_UNIT(.CENTI.,.METRE.)
);
#10520=(
NAMED_UNIT(*)
PLANE_ANGLE_UNIT()
SI_UNIT($,.RADIAN.)
);
#10521=(
NAMED_UNIT(*)
SI_UNIT($,.STERADIAN.)
SOLID_ANGLE_UNIT()
);
#10538=SHAPE_DEFINITION_REPRESENTATION(#10570,#10657);
#10570=PRODUCT_DEFINITION_SHAPE('',$,#10690);
#10657=SHAPE_REPRESENTATION('',(#6593),#10501);
#10673=PRODUCT_DEFINITION_CONTEXT('part definition',#10771,'design');
#10690=PRODUCT_DEFINITION('Flat Washer - M5','Flat Washer - M5',#10722,
#10673);
#10722=PRODUCT_DEFINITION_FORMATION('',$,#10789);
#10771=APPLICATION_CONTEXT(
'Core Data for Automotive Mechanical Design Process');
#10772=PRODUCT_CONTEXT('part definition',#10771,'mechanical');
#10789=PRODUCT('Flat Washer - M5','Flat Washer - M5','Flat Washer - M5',
(#10772));
#10875=COLOUR_RGB('Black',0.12,0.14,0.17);
#10876=FILL_AREA_STYLE_COLOUR('',#10875);
#10877=FILL_AREA_STYLE('',(#10876));
#10878=SURFACE_STYLE_FILL_AREA(#10877);
#10879=SURFACE_SIDE_STYLE('',(#10878));
#10880=SURFACE_STYLE_USAGE(.BOTH.,#10879);
#10881=PRESENTATION_STYLE_ASSIGNMENT((#10880));
ENDSEC;
END-ISO-10303-21;
